ISO-10303-21;
HEADER;
FILE_DESCRIPTION (('STEP AP214'),
    '1' );
FILE_NAME ('socket head cap screw_iso_ISO 4762 M12 x 80 - 36N.step',
    '2026-10-22T16:49:52',
    ( '' ),
    ( '' ),
    'SwSTEP 2.0',
    'SolidWorks 2026',
    '' );
FILE_SCHEMA (( 'AUTOMOTIVE_DESIGN' ));
ENDSEC;

DATA;
#1=CARTESIAN_POINT ( 'NONE',  ( 6.000000000000000000, 5.839897972853065333, -6.938893903907228378E-15 ) ) ;
#3=ADVANCED_FACE ( 'NONE', ( #4862, #2431 ), #2781, .T. ) ;
#5=ORIENTED_EDGE ( 'NONE', *, *, #3129, .F. ) ;
#15=DIRECTION ( 'NONE',  ( -1.000000000000000000, -0.000000000000000000, -0.000000000000000000 ) ) ;
#22=DIRECTION ( 'NONE',  ( -0.5000000000000046629, 1.060575238724903587E-16, -0.8660254037844359321 ) ) ;
#27=ORIENTED_EDGE ( 'NONE', *, *, #3576, .T. ) ;
#36=LINE ( 'NONE', #4185, #4654 ) ;
#38=TOROIDAL_SURFACE ( 'NONE', #2294, 6.600000000000001421, 0.5999999999999999778 ) ;
#41=ORIENTED_EDGE ( 'NONE', *, *, #794, .F. ) ;
#44=EDGE_LOOP ( 'NONE', ( #3924, #827, #3018, #2315, #3329 ) ) ;
#46=VECTOR ( 'NONE', #2795, 1000.000000000000000 ) ;
#58=ADVANCED_FACE ( 'NONE', ( #1562 ), #1695, .F. ) ;
#60=CIRCLE ( 'NONE', #4076, 6.600000000000001421 ) ;
#69=EDGE_CURVE ( 'NONE', #3352, #3493, #3834, .T. ) ;
#81=VERTEX_POINT ( 'NONE', #3427 ) ;
#83=LINE ( 'NONE', #4223, #2397 ) ;
#92=ORIENTED_EDGE ( 'NONE', *, *, #352, .F. ) ;
#93=DIRECTION ( 'NONE',  ( -1.000000000000000000, -0.000000000000000000, -0.000000000000000000 ) ) ;
#98=EDGE_CURVE ( 'NONE', #1888, #3300, #2243, .T. ) ;
#101=DIRECTION ( 'NONE',  ( 0.000000000000000000, 0.000000000000000000, 1.000000000000000000 ) ) ;
#110=EDGE_CURVE ( 'NONE', #2103, #3079, #2190, .T. ) ;
#122=AXIS2_PLACEMENT_3D ( 'NONE', #2468, #3586, #4820 ) ;
#125=CARTESIAN_POINT ( 'NONE',  ( 92.00000000000000000, 0.000000000000000000, 5.035999999999999588 ) ) ;
#139=EDGE_CURVE ( 'NONE', #2539, #1113, #5108, .T. ) ;
#142=CARTESIAN_POINT ( 'NONE',  ( 6.000000000000000000, 5.839897972853065333, -6.938893903907228378E-15 ) ) ;
#149=CARTESIAN_POINT ( 'NONE',  ( 0.000000000000000000, -2.919948986426539772, -5.057499999999996554 ) ) ;
#153=ORIENTED_EDGE ( 'NONE', *, *, #5054, .F. ) ;
#159=CARTESIAN_POINT ( 'NONE',  ( 6.000000000000000000, -5.258101095580057102E-15, -5.057500000000000107 ) ) ;
#167=EDGE_CURVE ( 'NONE', #2868, #5294, #475, .T. ) ;
#170=DIRECTION ( 'NONE',  ( 0.000000000000000000, -0.5000000000000012212, -0.8660254037844380415 ) ) ;
#178=( NAMED_UNIT ( * ) SI_UNIT ( $, .STERADIAN. ) SOLID_ANGLE_UNIT ( ) );
#189=DIRECTION ( 'NONE',  ( -1.000000000000000000, -0.000000000000000000, -0.000000000000000000 ) ) ;
#211=EDGE_CURVE ( 'NONE', #2103, #3135, #3145, .T. ) ;
#215=FILL_AREA_STYLE ('',( #650 ) ) ;
#219=CARTESIAN_POINT ( 'NONE',  ( 8.919948986426568638, 0.000000000000000000, 0.000000000000000000 ) ) ;
#241=AXIS2_PLACEMENT_3D ( 'NONE', #2577, #882, #3403 ) ;
#243=DIRECTION ( 'NONE',  ( -1.000000000000000000, -0.000000000000000000, -0.000000000000000000 ) ) ;
#246=CARTESIAN_POINT ( 'NONE',  ( 6.000000000000000000, -5.839897972853064445, 4.770489558936219510E-15 ) ) ;
#260=FACE_OUTER_BOUND ( 'NONE', #4753, .T. ) ;
#278=CYLINDRICAL_SURFACE ( 'NONE', #4326, 9.000000000000000000 ) ;
#281=ADVANCED_FACE ( 'NONE', ( #2796 ), #733, .T. ) ;
#294=EDGE_LOOP ( 'NONE', ( #2275, #2236, #92, #4689 ) ) ;
#304=AXIS2_PLACEMENT_3D ( 'NONE', #2018, #4467, #1392 ) ;
#314=VECTOR ( 'NONE', #1467, 1000.000000000000000 ) ;
#321=AXIS2_PLACEMENT_3D ( 'NONE', #748, #4422, #1239 ) ;
#326=CIRCLE ( 'NONE', #2598, 6.000000000000000888 ) ;
#329=ORIENTED_EDGE ( 'NONE', *, *, #2069, .F. ) ;
#338=VERTEX_POINT ( 'NONE', #418 ) ;
#341=DIRECTION ( 'NONE',  ( -0.000000000000000000, 1.188187522481193495E-15, 1.000000000000000000 ) ) ;
#352=EDGE_CURVE ( 'NONE', #3556, #1113, #326, .T. ) ;
#354=DIRECTION ( 'NONE',  ( 0.000000000000000000, 0.000000000000000000, -1.000000000000000000 ) ) ;
#365=EDGE_CURVE ( 'NONE', #3274, #4246, #3257, .T. ) ;
#366=VERTEX_POINT ( 'NONE', #1238 ) ;
#370=ORIENTED_EDGE ( 'NONE', *, *, #1420, .T. ) ;
#375=DIRECTION ( 'NONE',  ( 0.000000000000000000, 1.000000000000000000, -1.224646799147353207E-16 ) ) ;
#389=CARTESIAN_POINT ( 'NONE',  ( 6.000000000000000000, 5.839897972853065333, -6.938893903907228378E-15 ) ) ;
#404=ORIENTED_EDGE ( 'NONE', *, *, #632, .T. ) ;
#418=CARTESIAN_POINT ( 'NONE',  ( 0.000000000000000000, -5.839897972853064445, 4.770489558936219510E-15 ) ) ;
#421=CARTESIAN_POINT ( 'NONE',  ( 92.00000000000000000, 0.000000000000000000, 0.000000000000000000 ) ) ;
#449=ORIENTED_EDGE ( 'NONE', *, *, #2982, .F. ) ;
#461=FACE_OUTER_BOUND ( 'NONE', #710, .T. ) ;
#465=CARTESIAN_POINT ( 'NONE',  ( 0.000000000000000000, 2.919948986426526005, -5.057500000000002771 ) ) ;
#475=LINE ( 'NONE', #2130, #5231 ) ;
#481=AXIS2_PLACEMENT_3D ( 'NONE', #1, #2031, #1622 ) ;
#487=DIRECTION ( 'NONE',  ( 0.000000000000000000, 0.000000000000000000, 1.000000000000000000 ) ) ;
#512=ORIENTED_EDGE ( 'NONE', *, *, #139, .F. ) ;
#514=EDGE_LOOP ( 'NONE', ( #1436, #4747, #4585, #3936, #2557 ) ) ;
#539=VERTEX_POINT ( 'NONE', #3009 ) ;
#548=DIRECTION ( 'NONE',  ( 0.000000000000000000, -0.5000000000000012212, -0.8660254037844380415 ) ) ;
#552=AXIS2_PLACEMENT_3D ( 'NONE', #2520, #375, #1596 ) ;
#559=CARTESIAN_POINT ( 'NONE',  ( 6.000000000000000000, -2.919948986426526893, 5.057500000000001883 ) ) ;
#585=CARTESIAN_POINT ( 'NONE',  ( -31.74999999999995737, 0.000000000000000000, 0.000000000000000000 ) ) ;
#605=CARTESIAN_POINT ( 'NONE',  ( 6.000000000000000000, -2.919948986426539772, -5.057499999999996554 ) ) ;
#607=CARTESIAN_POINT ( 'NONE',  ( 12.59999999999999964, 0.000000000000000000, -6.600000000000001421 ) ) ;
#609=EDGE_CURVE ( 'NONE', #1113, #3556, #5351, .T. ) ;
#616=CARTESIAN_POINT ( 'NONE',  ( 91.03600000000004400, 7.347880794884120722E-16, -6.000000000000000888 ) ) ;
#617=DIRECTION ( 'NONE',  ( 0.000000000000000000, 0.000000000000000000, -1.000000000000000000 ) ) ;
#624=( NAMED_UNIT ( * ) SI_UNIT ( $, .STERADIAN. ) SOLID_ANGLE_UNIT ( ) );
#625=ORIENTED_EDGE ( 'NONE', *, *, #691, .T. ) ;
#630=CARTESIAN_POINT ( 'NONE',  ( 0.6000000000000033085, 1.102182119232617714E-15, -9.000000000000000000 ) ) ;
#631=EDGE_CURVE ( 'NONE', #4555, #366, #3353, .T. ) ;
#632=EDGE_CURVE ( 'NONE', #4595, #4480, #646, .T. ) ;
#636=AXIS2_PLACEMENT_3D ( 'NONE', #2673, #4331, #1507 ) ;
#643=ORIENTED_EDGE ( 'NONE', *, *, #4196, .T. ) ;
#644=AXIS2_PLACEMENT_3D ( 'NONE', #1226, #3354, #2903 ) ;
#646=LINE ( 'NONE', #1398, #2482 ) ;
#650=FILL_AREA_STYLE_COLOUR ( '', #1426 ) ;
#661=AXIS2_PLACEMENT_3D ( 'NONE', #1997, #4504, #3704 ) ;
#673=AXIS2_PLACEMENT_3D ( 'NONE', #2773, #341, #4135 ) ;
#678=DIRECTION ( 'NONE',  ( 0.000000000000000000, 0.000000000000000000, -1.000000000000000000 ) ) ;
#691=EDGE_CURVE ( 'NONE', #4457, #963, #1679, .T. ) ;
#695=DIRECTION ( 'NONE',  ( -1.000000000000000000, -0.000000000000000000, -0.000000000000000000 ) ) ;
#704=( NAMED_UNIT ( * ) PLANE_ANGLE_UNIT ( ) SI_UNIT ( $, .RADIAN. ) );
#710=EDGE_LOOP ( 'NONE', ( #1543, #1981, #3876, #3564 ) ) ;
#733=CONICAL_SURFACE ( 'NONE', #1585, 5.035999999999999588, 0.7853981633974743692 ) ;
#740=DIRECTION ( 'NONE',  ( 0.000000000000000000, 0.000000000000000000, 1.000000000000000000 ) ) ;
#748=CARTESIAN_POINT ( 'NONE',  ( 0.6000000000000033085, 0.000000000000000000, 0.000000000000000000 ) ) ;
#753=AXIS2_PLACEMENT_3D ( 'NONE', #421, #15, #1258 ) ;
#769=DIRECTION ( 'NONE',  ( 1.000000000000000000, 0.000000000000000000, 0.000000000000000000 ) ) ;
#771=VECTOR ( 'NONE', #4476, 1000.000000000000000 ) ;
#784=DIRECTION ( 'NONE',  ( -1.000000000000000000, -0.000000000000000000, -0.000000000000000000 ) ) ;
#785=CARTESIAN_POINT ( 'NONE',  ( 6.000000000000000000, 0.000000000000000000, 0.000000000000000000 ) ) ;
#787=EDGE_CURVE ( 'NONE', #1913, #3047, #981, .T. ) ;
#792=ORIENTED_EDGE ( 'NONE', *, *, #2169, .F. ) ;
#794=EDGE_CURVE ( 'NONE', #4433, #2174, #1143, .T. ) ;
#796=ORIENTED_EDGE ( 'NONE', *, *, #4341, .F. ) ;
#802=ADVANCED_FACE ( 'NONE', ( #1172 ), #38, .F. ) ;
#817=EDGE_CURVE ( 'NONE', #4457, #4555, #3001, .T. ) ;
#821=DIRECTION ( 'NONE',  ( -0.000000000000000000, 1.000000000000000000, 1.224646799147353207E-16 ) ) ;
#827=ORIENTED_EDGE ( 'NONE', *, *, #5184, .F. ) ;
#833=EDGE_LOOP ( 'NONE', ( #796, #4382, #5344, #886, #4460 ) ) ;
#835=DIRECTION ( 'NONE',  ( 0.000000000000000000, -0.4999999999999989453, 0.8660254037844392627 ) ) ;
#861=VECTOR ( 'NONE', #3140, 1000.000000000000000 ) ;
#866=FACE_OUTER_BOUND ( 'NONE', #2540, .T. ) ;
#882=DIRECTION ( 'NONE',  ( 0.000000000000000000, -1.039664082171044284E-15, -1.000000000000000000 ) ) ;
#886=ORIENTED_EDGE ( 'NONE', *, *, #1154, .T. ) ;
#888=ORIENTED_EDGE ( 'NONE', *, *, #961, .T. ) ;
#902=ORIENTED_EDGE ( 'NONE', *, *, #98, .F. ) ;
#916=( GEOMETRIC_REPRESENTATION_CONTEXT ( 3 ) GLOBAL_UNCERTAINTY_ASSIGNED_CONTEXT ( ( #2996 ) ) GLOBAL_UNIT_ASSIGNED_CONTEXT ( ( #5130, #4728, #624 ) ) REPRESENTATION_CONTEXT ( 'NONE', 'WORKASPACE' ) );
#940=EDGE_CURVE ( 'NONE', #1913, #5142, #3077, .T. ) ;
#941=ORIENTED_EDGE ( 'NONE', *, *, #1301, .T. ) ;
#948=DIRECTION ( 'NONE',  ( -1.000000000000000000, -0.000000000000000000, -0.000000000000000000 ) ) ;
#960=DIRECTION ( 'NONE',  ( 0.000000000000000000, -1.000000000000000000, 1.039664082171044284E-15 ) ) ;
#961=EDGE_CURVE ( 'NONE', #4929, #3556, #3052, .T. ) ;
#963=VERTEX_POINT ( 'NONE', #2198 ) ;
#964=ADVANCED_FACE ( 'NONE', ( #2979 ), #1321, .T. ) ;
#981=CIRCLE ( 'NONE', #552, 0.5999999999999998668 ) ;
#983=CARTESIAN_POINT ( 'NONE',  ( 6.000000000000000000, 5.839897972853065333, -6.938893903907228378E-15 ) ) ;
#987=TOROIDAL_SURFACE ( 'NONE', #2035, 6.600000000000001421, 0.5999999999999999778 ) ;
#994=DIRECTION ( 'NONE',  ( 0.000000000000000000, 0.8660254037844381525, -0.5000000000000008882 ) ) ;
#1001=ORIENTED_EDGE ( 'NONE', *, *, #1491, .F. ) ;
#1004=DIRECTION ( 'NONE',  ( -1.000000000000000000, -0.000000000000000000, -0.000000000000000000 ) ) ;
#1047=CARTESIAN_POINT ( 'NONE',  ( 0.000000000000000000, -2.919948986426526893, 5.057500000000001883 ) ) ;
#1056=CARTESIAN_POINT ( 'NONE',  ( 6.000000000000000000, -2.919948986426526893, 5.057500000000001883 ) ) ;
#1057=PLANE ( 'NONE',  #5183 ) ;
#1063=LINE ( 'NONE', #3084, #861 ) ;
#1070=FACE_OUTER_BOUND ( 'NONE', #3392, .T. ) ;
#1073=DIRECTION ( 'NONE',  ( -1.000000000000000000, -0.000000000000000000, -0.000000000000000000 ) ) ;
#1076=AXIS2_PLACEMENT_3D ( 'NONE', #3029, #3003, #101 ) ;
#1078=VECTOR ( 'NONE', #189, 1000.000000000000000 ) ;
#1087=CARTESIAN_POINT ( 'NONE',  ( 0.6000000000000033085, 0.000000000000000000, 0.000000000000000000 ) ) ;
#1110=VECTOR ( 'NONE', #22, 1000.000000000000000 ) ;
#1113=VERTEX_POINT ( 'NONE', #616 ) ;
#1118=DIRECTION ( 'NONE',  ( 1.000000000000000000, 0.000000000000000000, 0.000000000000000000 ) ) ;
#1121=DIRECTION ( 'NONE',  ( -1.000000000000000000, -0.000000000000000000, -0.000000000000000000 ) ) ;
#1130=CARTESIAN_POINT ( 'NONE',  ( 6.000000000000000000, -2.919948986426526893, 5.057500000000001883 ) ) ;
#1143=LINE ( 'NONE', #2909, #1406 ) ;
#1146=DIRECTION ( 'NONE',  ( -1.000000000000000000, -0.000000000000000000, -0.000000000000000000 ) ) ;
#1154=EDGE_CURVE ( 'NONE', #2898, #3300, #2654, .T. ) ;
#1172=FACE_OUTER_BOUND ( 'NONE', #3180, .T. ) ;
#1179=DIRECTION ( 'NONE',  ( -1.000000000000000000, -0.000000000000000000, -0.000000000000000000 ) ) ;
#1187=EDGE_LOOP ( 'NONE', ( #4986, #3605, #643, #4589 ) ) ;
#1202=EDGE_CURVE ( 'NONE', #539, #4595, #3574, .T. ) ;
#1207=DIRECTION ( 'NONE',  ( 0.000000000000000000, 0.000000000000000000, -1.000000000000000000 ) ) ;
#1210=PRODUCT_CONTEXT ( 'NONE', #2066, 'mechanical' ) ;
#1226=CARTESIAN_POINT ( 'NONE',  ( 6.000000000000000000, 0.000000000000000000, 0.000000000000000000 ) ) ;
#1238=CARTESIAN_POINT ( 'NONE',  ( 0.000000000000000000, 0.000000000000000000, 8.400000000000000355 ) ) ;
#1239=DIRECTION ( 'NONE',  ( 0.000000000000000000, 0.000000000000000000, 1.000000000000000000 ) ) ;
#1253=EDGE_CURVE ( 'NONE', #81, #3733, #3960, .T. ) ;
#1258=DIRECTION ( 'NONE',  ( 0.000000000000000000, 0.000000000000000000, 1.000000000000000000 ) ) ;
#1289=DIRECTION ( 'NONE',  ( 0.000000000000000000, 1.000000000000000000, -1.188187522481193495E-15 ) ) ;
#1301=EDGE_CURVE ( 'NONE', #338, #2174, #3008, .T. ) ;
#1303=DIRECTION ( 'NONE',  ( -0.7071067811865291430, 0.000000000000000000, 0.7071067811865660024 ) ) ;
#1312=( NAMED_UNIT ( * ) SI_UNIT ( $, .STERADIAN. ) SOLID_ANGLE_UNIT ( ) );
#1321=CYLINDRICAL_SURFACE ( 'NONE', #1076, 6.000000000000001776 ) ;
#1322=ADVANCED_FACE ( 'NONE', ( #5098 ), #987, .F. ) ;
#1326=CARTESIAN_POINT ( 'NONE',  ( 12.00000000000000000, 0.000000000000000000, 0.000000000000000000 ) ) ;
#1328=CARTESIAN_POINT ( 'NONE',  ( 11.99999999999999645, 0.000000000000000000, 0.000000000000000000 ) ) ;
#1333=AXIS2_PLACEMENT_3D ( 'NONE', #3641, #821, #2462 ) ;
#1349=CIRCLE ( 'NONE', #753, 5.035999999999999588 ) ;
#1364=CARTESIAN_POINT ( 'NONE',  ( 12.59999999999999964, 0.000000000000000000, 0.000000000000000000 ) ) ;
#1365=CARTESIAN_POINT ( 'NONE',  ( 92.00000000000000000, 6.167321280506070407E-16, -5.035999999999999588 ) ) ;
#1370=LINE ( 'NONE', #1734, #5092 ) ;
#1373=DIRECTION ( 'NONE',  ( -1.000000000000000000, -0.000000000000000000, -0.000000000000000000 ) ) ;
#1387=EDGE_CURVE ( 'NONE', #3047, #1861, #4637, .T. ) ;
#1392=DIRECTION ( 'NONE',  ( 0.000000000000000000, 0.000000000000000000, -1.000000000000000000 ) ) ;
#1398=CARTESIAN_POINT ( 'NONE',  ( 6.000000000000000000, -5.839897972853064445, 4.770489558936219510E-15 ) ) ;
#1401=ORIENTED_EDGE ( 'NONE', *, *, #2128, .T. ) ;
#1404=ORIENTED_EDGE ( 'NONE', *, *, #3129, .T. ) ;
#1406=VECTOR ( 'NONE', #4542, 1000.000000000000000 ) ;
#1416=ADVANCED_FACE ( 'NONE', ( #3065 ), #2212, .F. ) ;
#1417=EDGE_CURVE ( 'NONE', #81, #963, #3912, .T. ) ;
#1420=EDGE_CURVE ( 'NONE', #5142, #1913, #4815, .T. ) ;
#1426=COLOUR_RGB ( '',1.000000000000000000, 0.9490196078431372140, 0.9098039215686274384 ) ;
#1429=ORIENTED_EDGE ( 'NONE', *, *, #940, .F. ) ;
#1434=SURFACE_STYLE_USAGE ( .BOTH. , #3479 ) ;
#1436=ORIENTED_EDGE ( 'NONE', *, *, #2982, .T. ) ;
#1437=DIRECTION ( 'NONE',  ( 0.000000000000000000, 0.000000000000000000, -1.000000000000000000 ) ) ;
#1440=CIRCLE ( 'NONE', #3204, 9.000000000000000000 ) ;
#1441=CARTESIAN_POINT ( 'NONE',  ( 0.000000000000000000, -2.919948986426526893, 5.057500000000001883 ) ) ;
#1454=CARTESIAN_POINT ( 'NONE',  ( 0.000000000000000000, 0.000000000000000000, 0.000000000000000000 ) ) ;
#1467=DIRECTION ( 'NONE',  ( -1.000000000000000000, -0.000000000000000000, -0.000000000000000000 ) ) ;
#1473=ORIENTED_EDGE ( 'NONE', *, *, #5184, .T. ) ;
#1484=DIRECTION ( 'NONE',  ( 0.000000000000000000, 0.000000000000000000, 1.000000000000000000 ) ) ;
#1486=CARTESIAN_POINT ( 'NONE',  ( 6.000000000000000000, 5.839897972853065333, -6.938893903907228378E-15 ) ) ;
#1489=VERTEX_POINT ( 'NONE', #219 ) ;
#1491=EDGE_CURVE ( 'NONE', #2868, #3079, #2293, .T. ) ;
#1507=DIRECTION ( 'NONE',  ( 0.000000000000000000, 0.000000000000000000, 1.000000000000000000 ) ) ;
#1519=DIRECTION ( 'NONE',  ( -1.000000000000000000, -0.000000000000000000, -0.000000000000000000 ) ) ;
#1520=ORIENTED_EDGE ( 'NONE', *, *, #631, .T. ) ;
#1528=EDGE_CURVE ( 'NONE', #4480, #539, #3272, .T. ) ;
#1538=( LENGTH_UNIT ( ) NAMED_UNIT ( * ) SI_UNIT ( .MILLI., .METRE. ) );
#1543=ORIENTED_EDGE ( 'NONE', *, *, #4931, .F. ) ;
#1557=ADVANCED_FACE ( 'NONE', ( #1994 ), #2938, .F. ) ;
#1562=FACE_OUTER_BOUND ( 'NONE', #2292, .T. ) ;
#1569=CARTESIAN_POINT ( 'NONE',  ( 6.000000000000000000, 4.379923479639795225, -2.528750000000006271 ) ) ;
#1585=AXIS2_PLACEMENT_3D ( 'NONE', #2325, #1689, #4966 ) ;
#1588=AXIS2_PLACEMENT_3D ( 'NONE', #5017, #4274, #3772 ) ;
#1594=EDGE_CURVE ( 'NONE', #1113, #5142, #5246, .T. ) ;
#1596=DIRECTION ( 'NONE',  ( 0.000000000000000000, 1.224646799147354933E-16, 1.000000000000000000 ) ) ;
#1602=LINE ( 'NONE', #3289, #4144 ) ;
#1608=PLANE ( 'NONE',  #673 ) ;
#1622=DIRECTION ( 'NONE',  ( 0.000000000000000000, 0.000000000000000000, -1.000000000000000000 ) ) ;
#1627=EDGE_LOOP ( 'NONE', ( #3668, #4592, #625, #2747 ) ) ;
#1628=VECTOR ( 'NONE', #5025, 1000.000000000000000 ) ;
#1637=CIRCLE ( 'NONE', #2333, 5.035999999999999588 ) ;
#1644=FACE_OUTER_BOUND ( 'NONE', #2459, .T. ) ;
#1664=DIRECTION ( 'NONE',  ( -1.000000000000000000, -0.000000000000000000, -0.000000000000000000 ) ) ;
#1670=EDGE_CURVE ( 'NONE', #3556, #1913, #1602, .T. ) ;
#1679=CIRCLE ( 'NONE', #4634, 9.000000000000000000 ) ;
#1687=DIRECTION ( 'NONE',  ( -1.000000000000000000, -0.000000000000000000, -0.000000000000000000 ) ) ;
#1689=DIRECTION ( 'NONE',  ( -1.000000000000000000, -0.000000000000000000, -0.000000000000000000 ) ) ;
#1695=PLANE ( 'NONE',  #3064 ) ;
#1699=ADVANCED_FACE ( 'NONE', ( #3230 ), #4880, .F. ) ;
#1706=ADVANCED_FACE ( 'NONE', ( #4436 ), #1057, .F. ) ;
#1709=DIRECTION ( 'NONE',  ( 0.000000000000000000, -0.8660254037844391517, -0.4999999999999991118 ) ) ;
#1710=CIRCLE ( 'NONE', #4740, 9.000000000000000000 ) ;
#1711=AXIS2_PLACEMENT_3D ( 'NONE', #5126, #948, #2182 ) ;
#1715=CYLINDRICAL_SURFACE ( 'NONE', #4005, 9.000000000000000000 ) ;
#1721=DIRECTION ( 'NONE',  ( 0.000000000000000000, 0.000000000000000000, 1.000000000000000000 ) ) ;
#1729=DIRECTION ( 'NONE',  ( 0.000000000000000000, 0.000000000000000000, -1.000000000000000000 ) ) ;
#1734=CARTESIAN_POINT ( 'NONE',  ( 6.000000000000000000, -5.839897972853064445, 4.770489558936219510E-15 ) ) ;
#1738=DIRECTION ( 'NONE',  ( 0.000000000000000000, -0.5000000000000008882, -0.8660254037844380415 ) ) ;
#1747=ADVANCED_FACE ( 'NONE', ( #2671 ), #5120, .T. ) ;
#1752=DIRECTION ( 'NONE',  ( 1.000000000000000000, 0.000000000000000000, 0.000000000000000000 ) ) ;
#1756=PLANE ( 'NONE',  #3881 ) ;
#1760=PLANE ( 'NONE',  #3565 ) ;
#1762=EDGE_CURVE ( 'NONE', #3352, #539, #83, .T. ) ;
#1763=ADVANCED_FACE ( 'NONE', ( #3843 ), #2492, .F. ) ;
#1764=DIRECTION ( 'NONE',  ( 0.000000000000000000, 0.000000000000000000, -1.000000000000000000 ) ) ;
#1767=CARTESIAN_POINT ( 'NONE',  ( 12.00000000000000000, 8.082668874372532992E-16, 6.600000000000001421 ) ) ;
#1771=VECTOR ( 'NONE', #5024, 1000.000000000000000 ) ;
#1808=DIRECTION ( 'NONE',  ( 0.000000000000000000, 0.000000000000000000, 1.000000000000000000 ) ) ;
#1810=PRODUCT_DEFINITION_SHAPE ( 'NONE', 'NONE',  #4517 ) ;
#1818=LINE ( 'NONE', #5091, #2435 ) ;
#1819=MANIFOLD_SOLID_BREP ( 'Hex', #2750 ) ;
#1836=VECTOR ( 'NONE', #93, 1000.000000000000000 ) ;
#1837=ORIENTED_EDGE ( 'NONE', *, *, #4196, .F. ) ;
#1857=ORIENTED_EDGE ( 'NONE', *, *, #4656, .T. ) ;
#1861=VERTEX_POINT ( 'NONE', #3131 ) ;
#1868=ORIENTED_EDGE ( 'NONE', *, *, #1762, .F. ) ;
#1871=CARTESIAN_POINT ( 'NONE',  ( 0.000000000000000000, 2.919948986426538440, 5.057499999999994778 ) ) ;
#1873=PRESENTATION_STYLE_ASSIGNMENT (( #1434 ) ) ;
#1875=VECTOR ( 'NONE', #4339, 1000.000000000000000 ) ;
#1884=LINE ( 'NONE', #5250, #3116 ) ;
#1888=VERTEX_POINT ( 'NONE', #2723 ) ;
#1894=DIRECTION ( 'NONE',  ( -1.000000000000000000, -0.000000000000000000, -0.000000000000000000 ) ) ;
#1897=ADVANCED_FACE ( 'NONE', ( #260 ), #2009, .F. ) ;
#1904=SURFACE_STYLE_FILL_AREA ( #215 ) ;
#1907=DIRECTION ( 'NONE',  ( 0.000000000000000000, -0.4999999999999991118, 0.8660254037844390407 ) ) ;
#1911=DIRECTION ( 'NONE',  ( 0.000000000000000000, 0.000000000000000000, 1.000000000000000000 ) ) ;
#1913=VERTEX_POINT ( 'NONE', #4069 ) ;
#1917=VECTOR ( 'NONE', #548, 999.9999999999998863 ) ;
#1940=VECTOR ( 'NONE', #4016, 1000.000000000000227 ) ;
#1952=CARTESIAN_POINT ( 'NONE',  ( 6.000000000000000000, 6.009258394948634547E-15, 5.057499999999998330 ) ) ;
#1957=FACE_OUTER_BOUND ( 'NONE', #514, .T. ) ;
#1959=EDGE_CURVE ( 'NONE', #3274, #2898, #4312, .T. ) ;
#1965=FACE_OUTER_BOUND ( 'NONE', #2839, .T. ) ;
#1981=ORIENTED_EDGE ( 'NONE', *, *, #3699, .T. ) ;
#1994=FACE_OUTER_BOUND ( 'NONE', #833, .T. ) ;
#1997=CARTESIAN_POINT ( 'NONE',  ( 12.00000000000000000, 9.000000000000000000, 0.000000000000000000 ) ) ;
#2009=PLANE ( 'NONE',  #481 ) ;
#2018=CARTESIAN_POINT ( 'NONE',  ( 6.000000000000000000, 5.839897972853065333, -6.938893903907228378E-15 ) ) ;
#2027=ORIENTED_EDGE ( 'NONE', *, *, #2727, .T. ) ;
#2031=DIRECTION ( 'NONE',  ( 1.000000000000000000, 0.000000000000000000, 0.000000000000000000 ) ) ;
#2035=AXIS2_PLACEMENT_3D ( 'NONE', #3032, #3472, #1764 ) ;
#2045=DIRECTION ( 'NONE',  ( 0.000000000000000000, 0.5000000000000008882, 0.8660254037844381525 ) ) ;
#2053=PRODUCT_DEFINITION_FORMATION_WITH_SPECIFIED_SOURCE ( 'ANY', '', #2638, .NOT_KNOWN. ) ;
#2066=APPLICATION_CONTEXT ( 'automotive_design' ) ;
#2069=EDGE_CURVE ( 'NONE', #4480, #4433, #1370, .T. ) ;
#2103=VERTEX_POINT ( 'NONE', #3021 ) ;
#2121=AXIS2_PLACEMENT_3D ( 'NONE', #4524, #1519, #4027 ) ;
#2122=EDGE_LOOP ( 'NONE', ( #2653, #5131, #3837, #5147, #3884 ) ) ;
#2125=DIRECTION ( 'NONE',  ( 1.000000000000000000, 0.000000000000000000, 0.000000000000000000 ) ) ;
#2128=EDGE_CURVE ( 'NONE', #3079, #2174, #2998, .T. ) ;
#2130=CARTESIAN_POINT ( 'NONE',  ( 6.000000000000000000, 2.919948986426526005, -5.057500000000002771 ) ) ;
#2138=STYLED_ITEM ( 'NONE', ( #1873 ), #4176 ) ;
#2152=AXIS2_PLACEMENT_3D ( 'NONE', #607, #2274, #3536 ) ;
#2169=EDGE_CURVE ( 'NONE', #963, #366, #2579, .T. ) ;
#2174=VERTEX_POINT ( 'NONE', #149 ) ;
#2182=DIRECTION ( 'NONE',  ( 0.000000000000000000, 0.000000000000000000, 1.000000000000000000 ) ) ;
#2190=LINE ( 'NONE', #4683, #1917 ) ;
#2194=DIRECTION ( 'NONE',  ( 0.000000000000000000, -1.000000000000000000, 0.000000000000000000 ) ) ;
#2195=ADVANCED_FACE ( 'NONE', ( #4216 ), #1756, .T. ) ;
#2198=CARTESIAN_POINT ( 'NONE',  ( 0.6000000000000033085, 0.000000000000000000, 9.000000000000000000 ) ) ;
#2199=DIRECTION ( 'NONE',  ( -1.000000000000000000, -0.000000000000000000, -0.000000000000000000 ) ) ;
#2210=AXIS2_PLACEMENT_3D ( 'NONE', #1364, #3526, #5185 ) ;
#2212=PLANE ( 'NONE',  #3440 ) ;
#2214=DIRECTION ( 'NONE',  ( 0.000000000000000000, -1.000000000000000000, 1.039664082171044284E-15 ) ) ;
#2223=ORIENTED_EDGE ( 'NONE', *, *, #2169, .T. ) ;
#2236=ORIENTED_EDGE ( 'NONE', *, *, #139, .T. ) ;
#2238=CARTESIAN_POINT ( 'NONE',  ( 92.00000000000000000, 0.000000000000000000, 5.035999999999999588 ) ) ;
#2241=TOROIDAL_SURFACE ( 'NONE', #3743, 8.400000000000000355, 0.5999999999999999778 ) ;
#2243=LINE ( 'NONE', #983, #2627 ) ;
#2264=SHAPE_REPRESENTATION_RELATIONSHIP ( 'NONE' , 'NONE' ,  #2934, #4176 ) ;
#2266=ADVANCED_FACE ( 'NONE', ( #3150 ), #2331, .F. ) ;
#2274=DIRECTION ( 'NONE',  ( 0.000000000000000000, -1.000000000000000000, 0.000000000000000000 ) ) ;
#2275=ORIENTED_EDGE ( 'NONE', *, *, #5054, .T. ) ;
#2287=ORIENTED_EDGE ( 'NONE', *, *, #1594, .T. ) ;
#2292=EDGE_LOOP ( 'NONE', ( #1868, #3111, #2396 ) ) ;
#2293=LINE ( 'NONE', #3453, #4061 ) ;
#2294=AXIS2_PLACEMENT_3D ( 'NONE', #4960, #4519, #354 ) ;
#2298=ADVANCED_FACE ( 'NONE', ( #4324 ), #3595, .T. ) ;
#2300=AXIS2_PLACEMENT_3D ( 'NONE', #1326, #1687, #4649 ) ;
#2315=ORIENTED_EDGE ( 'NONE', *, *, #3447, .T. ) ;
#2325=CARTESIAN_POINT ( 'NONE',  ( 92.00000000000000000, 0.000000000000000000, 0.000000000000000000 ) ) ;
#2331=PLANE ( 'NONE',  #2412 ) ;
#2333=AXIS2_PLACEMENT_3D ( 'NONE', #3196, #1121, #2790 ) ;
#2346=ORIENTED_EDGE ( 'NONE', *, *, #211, .T. ) ;
#2356=DIRECTION ( 'NONE',  ( 0.000000000000000000, 0.000000000000000000, -1.000000000000000000 ) ) ;
#2375=PLANE ( 'NONE',  #2861 ) ;
#2377=UNCERTAINTY_MEASURE_WITH_UNIT (LENGTH_MEASURE( 1.000000000000000082E-05 ), #1538, 'distance_accuracy_value', 'NONE');
#2384=FACE_OUTER_BOUND ( 'NONE', #1627, .T. ) ;
#2396=ORIENTED_EDGE ( 'NONE', *, *, #3766, .F. ) ;
#2397=VECTOR ( 'NONE', #1738, 1000.000000000000227 ) ;
#2400=EDGE_LOOP ( 'NONE', ( #5036, #4952, #2889, #5202, #1404 ) ) ;
#2412=AXIS2_PLACEMENT_3D ( 'NONE', #5221, #4798, #3535 ) ;
#2418=FACE_BOUND ( 'NONE', #5367, .T. ) ;
#2422=VECTOR ( 'NONE', #3914, 1000.000000000000114 ) ;
#2431=FACE_OUTER_BOUND ( 'NONE', #4868, .T. ) ;
#2434=CARTESIAN_POINT ( 'NONE',  ( 0.000000000000000000, 0.000000000000000000, 0.000000000000000000 ) ) ;
#2435=VECTOR ( 'NONE', #2620, 1000.000000000000000 ) ;
#2459=EDGE_LOOP ( 'NONE', ( #512, #3271, #888, #4241 ) ) ;
#2462=DIRECTION ( 'NONE',  ( 0.000000000000000000, -1.224646799147353207E-16, 1.000000000000000000 ) ) ;
#2468=CARTESIAN_POINT ( 'NONE',  ( 6.000000000000000000, 0.000000000000000000, 0.000000000000000000 ) ) ;
#2471=DIRECTION ( 'NONE',  ( 0.000000000000000000, 0.000000000000000000, 1.000000000000000000 ) ) ;
#2482=VECTOR ( 'NONE', #3550, 1000.000000000000000 ) ;
#2492=CONICAL_SURFACE ( 'NONE', #3525, 5.057500000000000107, 1.047197551196592302 ) ;
#2496=CARTESIAN_POINT ( 'NONE',  ( 91.03600000000004400, 0.000000000000000000, 0.000000000000000000 ) ) ;
#2504=ORIENTED_EDGE ( 'NONE', *, *, #1202, .F. ) ;
#2513=ORIENTED_EDGE ( 'NONE', *, *, #3038, .F. ) ;
#2520=CARTESIAN_POINT ( 'NONE',  ( 12.59999999999999964, 8.082668874372532992E-16, 6.600000000000001421 ) ) ;
#2533=CARTESIAN_POINT ( 'NONE',  ( 6.000000000000000000, -5.839897972853064445, 4.770489558936219510E-15 ) ) ;
#2539=VERTEX_POINT ( 'NONE', #4244 ) ;
#2540=EDGE_LOOP ( 'NONE', ( #4104, #5, #404, #4888, #4096 ) ) ;
#2555=( NAMED_UNIT ( * ) PLANE_ANGLE_UNIT ( ) SI_UNIT ( $, .RADIAN. ) );
#2557=ORIENTED_EDGE ( 'NONE', *, *, #69, .T. ) ;
#2577=CARTESIAN_POINT ( 'NONE',  ( 6.000000000000000000, 2.919948986426526005, -5.057500000000002771 ) ) ;
#2579=CIRCLE ( 'NONE', #4148, 0.5999999999999998668 ) ;
#2583=CARTESIAN_POINT ( 'NONE',  ( 6.000000000000000000, -2.919948986426526893, 5.057500000000001883 ) ) ;
#2598=AXIS2_PLACEMENT_3D ( 'NONE', #2496, #4111, #3755 ) ;
#2616=ORIENTED_EDGE ( 'NONE', *, *, #4297, .T. ) ;
#2620=DIRECTION ( 'NONE',  ( -1.000000000000000000, -0.000000000000000000, -0.000000000000000000 ) ) ;
#2627=VECTOR ( 'NONE', #170, 999.9999999999998863 ) ;
#2638=PRODUCT ( 'socket head cap screw_iso_ISO 4762 M12 x 80 - 36N', 'socket head cap screw_iso_ISO 4762 M12 x 80 - 36N', '', ( #1210 ) ) ;
#2643=DIRECTION ( 'NONE',  ( -1.000000000000000000, -0.000000000000000000, -0.000000000000000000 ) ) ;
#2653=ORIENTED_EDGE ( 'NONE', *, *, #5006, .F. ) ;
#2654=CIRCLE ( 'NONE', #4387, 5.057500000000000107 ) ;
#2662=EDGE_CURVE ( 'NONE', #4246, #3135, #5136, .T. ) ;
#2668=AXIS2_PLACEMENT_3D ( 'NONE', #585, #1073, #1911 ) ;
#2671=FACE_OUTER_BOUND ( 'NONE', #2400, .T. ) ;
#2673=CARTESIAN_POINT ( 'NONE',  ( 11.99999999999999645, 0.000000000000000000, 0.000000000000000000 ) ) ;
#2675=FACE_OUTER_BOUND ( 'NONE', #4210, .T. ) ;
#2706=ORIENTED_EDGE ( 'NONE', *, *, #4529, .F. ) ;
#2722=EDGE_LOOP ( 'NONE', ( #2706, #3917, #3673 ) ) ;
#2723=CARTESIAN_POINT ( 'NONE',  ( 6.000000000000000000, 5.839897972853065333, -6.938893903907228378E-15 ) ) ;
#2727=EDGE_CURVE ( 'NONE', #3493, #338, #5159, .T. ) ;
#2741=CARTESIAN_POINT ( 'NONE',  ( 0.6000000000000033085, 0.000000000000000000, 0.000000000000000000 ) ) ;
#2747=ORIENTED_EDGE ( 'NONE', *, *, #1417, .F. ) ;
#2750=CLOSED_SHELL ( 'NONE', ( #1763, #2836, #802, #281, #964, #3594, #3, #5181, #2904, #2298, #2813, #5268, #1322, #4546, #2195, #4641, #1747, #4402, #4712, #2266, #1897, #1416, #58, #1706, #1699, #3318, #1557 ) ) ;
#2773=CARTESIAN_POINT ( 'NONE',  ( 6.000000000000000000, -2.919948986426526893, 5.057500000000001883 ) ) ;
#2781=PLANE ( 'NONE',  #5014 ) ;
#2790=DIRECTION ( 'NONE',  ( 0.000000000000000000, 0.000000000000000000, 1.000000000000000000 ) ) ;
#2795=DIRECTION ( 'NONE',  ( -1.000000000000000000, -0.000000000000000000, -0.000000000000000000 ) ) ;
#2796=FACE_OUTER_BOUND ( 'NONE', #294, .T. ) ;
#2798=DIRECTION ( 'NONE',  ( 0.000000000000000000, 0.000000000000000000, 1.000000000000000000 ) ) ;
#2799=DIRECTION ( 'NONE',  ( 0.000000000000000000, 1.000000000000000000, -1.188187522481193495E-15 ) ) ;
#2803=ORIENTED_EDGE ( 'NONE', *, *, #632, .F. ) ;
#2810=ORIENTED_EDGE ( 'NONE', *, *, #1670, .T. ) ;
#2813=ADVANCED_FACE ( 'NONE', ( #1644 ), #4926, .T. ) ;
#2826=VECTOR ( 'NONE', #1303, 1000.000000000000000 ) ;
#2830=LINE ( 'NONE', #4452, #771 ) ;
#2836=ADVANCED_FACE ( 'NONE', ( #3293 ), #3378, .T. ) ;
#2839=EDGE_LOOP ( 'NONE', ( #1401, #41, #5005, #3370, #4197 ) ) ;
#2844=EDGE_LOOP ( 'NONE', ( #2803, #2504, #3241 ) ) ;
#2853=( GEOMETRIC_REPRESENTATION_CONTEXT ( 3 ) GLOBAL_UNCERTAINTY_ASSIGNED_CONTEXT ( ( #3044 ) ) GLOBAL_UNIT_ASSIGNED_CONTEXT ( ( #5031, #2555, #1312 ) ) REPRESENTATION_CONTEXT ( 'NONE', 'WORKASPACE' ) );
#2861=AXIS2_PLACEMENT_3D ( 'NONE', #1486, #3643, #1207 ) ;
#2868=VERTEX_POINT ( 'NONE', #3678 ) ;
#2889=ORIENTED_EDGE ( 'NONE', *, *, #1762, .T. ) ;
#2893=DIRECTION ( 'NONE',  ( 0.000000000000000000, 0.000000000000000000, 1.000000000000000000 ) ) ;
#2896=EDGE_CURVE ( 'NONE', #3300, #5294, #4834, .T. ) ;
#2898=VERTEX_POINT ( 'NONE', #4968 ) ;
#2903=DIRECTION ( 'NONE',  ( 0.000000000000000000, 0.000000000000000000, 1.000000000000000000 ) ) ;
#2904=ADVANCED_FACE ( 'NONE', ( #2418, #4088 ), #4942, .T. ) ;
#2908=ORIENTED_EDGE ( 'NONE', *, *, #691, .F. ) ;
#2909=CARTESIAN_POINT ( 'NONE',  ( 6.000000000000000000, -2.919948986426539772, -5.057499999999996554 ) ) ;
#2927=EDGE_LOOP ( 'NONE', ( #5310, #4777, #2810, #4852 ) ) ;
#2934=SHAPE_REPRESENTATION ( 'socket head cap screw_iso_ISO 4762 M12 x 80 - 36N', ( #4154 ), #2853 ) ;
#2938=CONICAL_SURFACE ( 'NONE', #122, 5.057500000000000107, 1.047197551196592302 ) ;
#2948=ORIENTED_EDGE ( 'NONE', *, *, #1387, .T. ) ;
#2955=EDGE_CURVE ( 'NONE', #963, #4457, #1710, .T. ) ;
#2972=PLANE ( 'NONE',  #4090 ) ;
#2979=FACE_OUTER_BOUND ( 'NONE', #5232, .T. ) ;
#2982=EDGE_CURVE ( 'NONE', #3493, #3135, #36, .T. ) ;
#2996=UNCERTAINTY_MEASURE_WITH_UNIT (LENGTH_MEASURE( 1.000000000000000082E-05 ), #5130, 'distance_accuracy_value', 'NONE');
#2998=LINE ( 'NONE', #4194, #3450 ) ;
#3001=CIRCLE ( 'NONE', #1333, 0.5999999999999998668 ) ;
#3003=DIRECTION ( 'NONE',  ( -1.000000000000000000, -0.000000000000000000, -0.000000000000000000 ) ) ;
#3008=LINE ( 'NONE', #3369, #1771 ) ;
#3009=CARTESIAN_POINT ( 'NONE',  ( 6.000000000000000000, -4.379923479639794337, 2.528750000000003606 ) ) ;
#3012=ORIENTED_EDGE ( 'NONE', *, *, #2955, .F. ) ;
#3018=ORIENTED_EDGE ( 'NONE', *, *, #4529, .T. ) ;
#3021=CARTESIAN_POINT ( 'NONE',  ( 0.000000000000000000, 5.839897972853065333, -6.938893903907228378E-15 ) ) ;
#3029=CARTESIAN_POINT ( 'NONE',  ( -31.74999999999995737, 0.000000000000000000, 0.000000000000000000 ) ) ;
#3030=CARTESIAN_POINT ( 'NONE',  ( 92.00000000000000000, 5.035999999999999588, 0.000000000000000000 ) ) ;
#3032=CARTESIAN_POINT ( 'NONE',  ( 12.59999999999999964, 0.000000000000000000, 0.000000000000000000 ) ) ;
#3038=EDGE_CURVE ( 'NONE', #2539, #4929, #1349, .T. ) ;
#3044=UNCERTAINTY_MEASURE_WITH_UNIT (LENGTH_MEASURE( 1.000000000000000082E-05 ), #5031, 'distance_accuracy_value', 'NONE');
#3047=VERTEX_POINT ( 'NONE', #1767 ) ;
#3052=LINE ( 'NONE', #125, #2826 ) ;
#3064=AXIS2_PLACEMENT_3D ( 'NONE', #5157, #1752, #1729 ) ;
#3065=FACE_OUTER_BOUND ( 'NONE', #2844, .T. ) ;
#3077=CIRCLE ( 'NONE', #1588, 6.000000000000001776 ) ;
#3079=VERTEX_POINT ( 'NONE', #465 ) ;
#3083=EDGE_LOOP ( 'NONE', ( #2346, #449, #2027, #941, #3987, #3719 ) ) ;
#3084=CARTESIAN_POINT ( 'NONE',  ( -31.74999999999995737, 1.102182119232617714E-15, -9.000000000000000000 ) ) ;
#3106=DIRECTION ( 'NONE',  ( 1.000000000000000000, 0.000000000000000000, 0.000000000000000000 ) ) ;
#3109=APPLICATION_CONTEXT ( 'automotive_design' ) ;
#3111=ORIENTED_EDGE ( 'NONE', *, *, #4698, .T. ) ;
#3116=VECTOR ( 'NONE', #3124, 1000.000000000000114 ) ;
#3123=DIRECTION ( 'NONE',  ( 0.000000000000000000, -0.5000000000000008882, -0.8660254037844380415 ) ) ;
#3124=DIRECTION ( 'NONE',  ( 0.000000000000000000, -0.4999999999999991118, 0.8660254037844390407 ) ) ;
#3129=EDGE_CURVE ( 'NONE', #4595, #338, #3521, .T. ) ;
#3131=CARTESIAN_POINT ( 'NONE',  ( 12.00000000000000000, 0.000000000000000000, -6.600000000000001421 ) ) ;
#3133=DIRECTION ( 'NONE',  ( 0.000000000000000000, 0.000000000000000000, 1.000000000000000000 ) ) ;
#3135=VERTEX_POINT ( 'NONE', #1871 ) ;
#3140=DIRECTION ( 'NONE',  ( -1.000000000000000000, -0.000000000000000000, -0.000000000000000000 ) ) ;
#3145=LINE ( 'NONE', #3588, #4531 ) ;
#3150=FACE_OUTER_BOUND ( 'NONE', #3165, .T. ) ;
#3160=FACE_OUTER_BOUND ( 'NONE', #4913, .T. ) ;
#3165=EDGE_LOOP ( 'NONE', ( #3278, #1001, #3220, #902, #1473 ) ) ;
#3180=EDGE_LOOP ( 'NONE', ( #1429, #3341, #4444, #1837 ) ) ;
#3187=CARTESIAN_POINT ( 'NONE',  ( 6.000000000000000000, 5.839897972853065333, -6.938893903907228378E-15 ) ) ;
#3196=CARTESIAN_POINT ( 'NONE',  ( 92.00000000000000000, 0.000000000000000000, 0.000000000000000000 ) ) ;
#3204=AXIS2_PLACEMENT_3D ( 'NONE', #1328, #1664, #1721 ) ;
#3206=LINE ( 'NONE', #1130, #3307 ) ;
#3212=CIRCLE ( 'NONE', #5303, 5.057500000000000107 ) ;
#3213=ORIENTED_EDGE ( 'NONE', *, *, #5105, .F. ) ;
#3220=ORIENTED_EDGE ( 'NONE', *, *, #4656, .F. ) ;
#3227=CARTESIAN_POINT ( 'NONE',  ( 6.000000000000000000, 0.000000000000000000, 0.000000000000000000 ) ) ;
#3229=ORIENTED_EDGE ( 'NONE', *, *, #3447, .F. ) ;
#3230=FACE_OUTER_BOUND ( 'NONE', #2722, .T. ) ;
#3233=DIRECTION ( 'NONE',  ( -1.000000000000000000, -0.000000000000000000, -0.000000000000000000 ) ) ;
#3241=ORIENTED_EDGE ( 'NONE', *, *, #1528, .F. ) ;
#3257=LINE ( 'NONE', #4940, #1628 ) ;
#3271=ORIENTED_EDGE ( 'NONE', *, *, #3038, .T. ) ;
#3272=CIRCLE ( 'NONE', #2121, 5.057500000000000107 ) ;
#3274=VERTEX_POINT ( 'NONE', #1952 ) ;
#3278=ORIENTED_EDGE ( 'NONE', *, *, #110, .T. ) ;
#3289=CARTESIAN_POINT ( 'NONE',  ( -31.74999999999995737, 0.000000000000000000, 6.000000000000001776 ) ) ;
#3293=FACE_OUTER_BOUND ( 'NONE', #4603, .T. ) ;
#3294=CARTESIAN_POINT ( 'NONE',  ( 6.000000000000000000, -5.839897972853064445, 4.770489558936219510E-15 ) ) ;
#3300=VERTEX_POINT ( 'NONE', #1569 ) ;
#3307=VECTOR ( 'NONE', #2799, 1000.000000000000000 ) ;
#3316=CARTESIAN_POINT ( 'NONE',  ( 12.59999999999999964, 7.347880794884121708E-16, -6.000000000000001776 ) ) ;
#3318=ADVANCED_FACE ( 'NONE', ( #3160 ), #2375, .F. ) ;
#3329=ORIENTED_EDGE ( 'NONE', *, *, #2662, .T. ) ;
#3341=ORIENTED_EDGE ( 'NONE', *, *, #787, .T. ) ;
#3352=VERTEX_POINT ( 'NONE', #4813 ) ;
#3353=CIRCLE ( 'NONE', #5083, 8.400000000000000355 ) ;
#3354=DIRECTION ( 'NONE',  ( -1.000000000000000000, -0.000000000000000000, -0.000000000000000000 ) ) ;
#3369=CARTESIAN_POINT ( 'NONE',  ( 0.000000000000000000, -5.839897972853064445, 4.770489558936219510E-15 ) ) ;
#3370=ORIENTED_EDGE ( 'NONE', *, *, #167, .F. ) ;
#3378=TOROIDAL_SURFACE ( 'NONE', #321, 8.400000000000000355, 0.5999999999999999778 ) ;
#3392=EDGE_LOOP ( 'NONE', ( #5366, #3012, #2223, #5051 ) ) ;
#3395=CARTESIAN_POINT ( 'NONE',  ( -31.74999999999995737, 0.000000000000000000, 0.000000000000000000 ) ) ;
#3403=DIRECTION ( 'NONE',  ( 0.000000000000000000, 1.000000000000000000, -1.039664082171044284E-15 ) ) ;
#3427=CARTESIAN_POINT ( 'NONE',  ( 11.99999999999999645, 0.000000000000000000, 9.000000000000000000 ) ) ;
#3439=DIRECTION ( 'NONE',  ( 0.000000000000000000, 0.000000000000000000, 1.000000000000000000 ) ) ;
#3440=AXIS2_PLACEMENT_3D ( 'NONE', #142, #4793, #1437 ) ;
#3445=CARTESIAN_POINT ( 'NONE',  ( 11.99999999999999645, 1.102182119232617714E-15, -9.000000000000000000 ) ) ;
#3447=EDGE_CURVE ( 'NONE', #2898, #4246, #3503, .T. ) ;
#3450=VECTOR ( 'NONE', #960, 1000.000000000000000 ) ;
#3453=CARTESIAN_POINT ( 'NONE',  ( 6.000000000000000000, 2.919948986426526005, -5.057500000000002771 ) ) ;
#3468=CARTESIAN_POINT ( 'NONE',  ( 6.000000000000000000, 0.000000000000000000, 0.000000000000000000 ) ) ;
#3472=DIRECTION ( 'NONE',  ( 1.000000000000000000, 0.000000000000000000, 0.000000000000000000 ) ) ;
#3479=SURFACE_SIDE_STYLE ('',( #1904 ) ) ;
#3493=VERTEX_POINT ( 'NONE', #1047 ) ;
#3502=DIRECTION ( 'NONE',  ( -0.7071067811865291430, 8.659560562355159656E-17, -0.7071067811865660024 ) ) ;
#3503=LINE ( 'NONE', #4684, #2422 ) ;
#3513=DIRECTION ( 'NONE',  ( 0.000000000000000000, 0.000000000000000000, 1.000000000000000000 ) ) ;
#3521=LINE ( 'NONE', #246, #1875 ) ;
#3525=AXIS2_PLACEMENT_3D ( 'NONE', #3468, #1373, #487 ) ;
#3526=DIRECTION ( 'NONE',  ( 1.000000000000000000, 0.000000000000000000, 0.000000000000000000 ) ) ;
#3535=DIRECTION ( 'NONE',  ( 0.000000000000000000, 0.5000000000000012212, 0.8660254037844379305 ) ) ;
#3536=DIRECTION ( 'NONE',  ( 0.000000000000000000, 0.000000000000000000, -1.000000000000000000 ) ) ;
#3550=DIRECTION ( 'NONE',  ( 0.000000000000000000, 0.4999999999999990008, -0.8660254037844392627 ) ) ;
#3556=VERTEX_POINT ( 'NONE', #4367 ) ;
#3557=VECTOR ( 'NONE', #3736, 999.9999999999998863 ) ;
#3563=CARTESIAN_POINT ( 'NONE',  ( 0.000000000000000000, 1.065442715258197248E-15, -8.400000000000000355 ) ) ;
#3564=ORIENTED_EDGE ( 'NONE', *, *, #2955, .T. ) ;
#3565=AXIS2_PLACEMENT_3D ( 'NONE', #3030, #3106, #617 ) ;
#3574=LINE ( 'NONE', #1056, #1940 ) ;
#3576=EDGE_CURVE ( 'NONE', #1861, #3047, #60, .T. ) ;
#3584=VECTOR ( 'NONE', #3502, 1000.000000000000000 ) ;
#3586=DIRECTION ( 'NONE',  ( -1.000000000000000000, -0.000000000000000000, -0.000000000000000000 ) ) ;
#3588=CARTESIAN_POINT ( 'NONE',  ( 0.000000000000000000, 5.839897972853065333, -6.938893903907228378E-15 ) ) ;
#3594=ADVANCED_FACE ( 'NONE', ( #2384 ), #278, .T. ) ;
#3595=CYLINDRICAL_SURFACE ( 'NONE', #2668, 6.000000000000001776 ) ;
#3605=ORIENTED_EDGE ( 'NONE', *, *, #1420, .F. ) ;
#3606=CARTESIAN_POINT ( 'NONE',  ( 0.000000000000000000, 0.000000000000000000, 0.000000000000000000 ) ) ;
#3609=CARTESIAN_POINT ( 'NONE',  ( 6.000000000000000000, 0.000000000000000000, 5.057500000000000107 ) ) ;
#3641=CARTESIAN_POINT ( 'NONE',  ( 0.6000000000000033085, 1.028703311283776586E-15, -8.400000000000000355 ) ) ;
#3643=DIRECTION ( 'NONE',  ( 1.000000000000000000, 0.000000000000000000, 0.000000000000000000 ) ) ;
#3656=PLANE ( 'NONE',  #241 ) ;
#3668=ORIENTED_EDGE ( 'NONE', *, *, #1253, .T. ) ;
#3673=ORIENTED_EDGE ( 'NONE', *, *, #1154, .F. ) ;
#3675=ORIENTED_EDGE ( 'NONE', *, *, #365, .T. ) ;
#3677=CARTESIAN_POINT ( 'NONE',  ( 12.00000000000000000, 0.000000000000000000, 0.000000000000000000 ) ) ;
#3678=CARTESIAN_POINT ( 'NONE',  ( 6.000000000000000000, 2.919948986426526005, -5.057500000000002771 ) ) ;
#3682=EDGE_LOOP ( 'NONE', ( #4410, #4783 ) ) ;
#3699=EDGE_CURVE ( 'NONE', #3733, #81, #1440, .T. ) ;
#3704=DIRECTION ( 'NONE',  ( 0.000000000000000000, 0.000000000000000000, -1.000000000000000000 ) ) ;
#3719=ORIENTED_EDGE ( 'NONE', *, *, #110, .F. ) ;
#3733=VERTEX_POINT ( 'NONE', #3445 ) ;
#3736=DIRECTION ( 'NONE',  ( 0.000000000000000000, -0.5000000000000012212, -0.8660254037844380415 ) ) ;
#3742=EDGE_LOOP ( 'NONE', ( #3675, #3229, #4177 ) ) ;
#3743=AXIS2_PLACEMENT_3D ( 'NONE', #2741, #3888, #1808 ) ;
#3755=DIRECTION ( 'NONE',  ( 0.000000000000000000, 0.000000000000000000, 1.000000000000000000 ) ) ;
#3766=EDGE_CURVE ( 'NONE', #539, #3274, #5293, .T. ) ;
#3772=DIRECTION ( 'NONE',  ( 0.000000000000000000, 0.000000000000000000, -1.000000000000000000 ) ) ;
#3794=ORIENTED_EDGE ( 'NONE', *, *, #1670, .F. ) ;
#3826=AXIS2_PLACEMENT_3D ( 'NONE', #1454, #2199, #3513 ) ;
#3831=DIRECTION ( 'NONE',  ( 0.000000000000000000, 0.000000000000000000, 1.000000000000000000 ) ) ;
#3834=LINE ( 'NONE', #2583, #1836 ) ;
#3837=ORIENTED_EDGE ( 'NONE', *, *, #5105, .T. ) ;
#3843=FACE_OUTER_BOUND ( 'NONE', #2122, .T. ) ;
#3876=ORIENTED_EDGE ( 'NONE', *, *, #1417, .T. ) ;
#3881=AXIS2_PLACEMENT_3D ( 'NONE', #4688, #1709, #4594 ) ;
#3884=ORIENTED_EDGE ( 'NONE', *, *, #3766, .T. ) ;
#3888=DIRECTION ( 'NONE',  ( -1.000000000000000000, -0.000000000000000000, -0.000000000000000000 ) ) ;
#3912=LINE ( 'NONE', #3963, #1078 ) ;
#3914=DIRECTION ( 'NONE',  ( 0.000000000000000000, -0.4999999999999991118, 0.8660254037844390407 ) ) ;
#3917=ORIENTED_EDGE ( 'NONE', *, *, #98, .T. ) ;
#3924=ORIENTED_EDGE ( 'NONE', *, *, #211, .F. ) ;
#3929=ORIENTED_EDGE ( 'NONE', *, *, #167, .T. ) ;
#3930=DIRECTION ( 'NONE',  ( 0.000000000000000000, 0.000000000000000000, 1.000000000000000000 ) ) ;
#3936=ORIENTED_EDGE ( 'NONE', *, *, #4698, .F. ) ;
#3960=CIRCLE ( 'NONE', #636, 9.000000000000000000 ) ;
#3963=CARTESIAN_POINT ( 'NONE',  ( -31.74999999999995737, 0.000000000000000000, 9.000000000000000000 ) ) ;
#3978=AXIS2_PLACEMENT_3D ( 'NONE', #4470, #4910, #2471 ) ;
#3987=ORIENTED_EDGE ( 'NONE', *, *, #2128, .F. ) ;
#4005=AXIS2_PLACEMENT_3D ( 'NONE', #3395, #2643, #3439 ) ;
#4016=DIRECTION ( 'NONE',  ( 0.000000000000000000, -0.5000000000000008882, -0.8660254037844380415 ) ) ;
#4027=DIRECTION ( 'NONE',  ( 0.000000000000000000, 0.000000000000000000, 1.000000000000000000 ) ) ;
#4061=VECTOR ( 'NONE', #4364, 1000.000000000000000 ) ;
#4068=DIRECTION ( 'NONE',  ( -0.000000000000000000, 0.000000000000000000, 1.000000000000000000 ) ) ;
#4069=CARTESIAN_POINT ( 'NONE',  ( 12.59999999999999964, 0.000000000000000000, 6.000000000000001776 ) ) ;
#4076=AXIS2_PLACEMENT_3D ( 'NONE', #3677, #695, #2356 ) ;
#4088=FACE_OUTER_BOUND ( 'NONE', #3682, .T. ) ;
#4090=AXIS2_PLACEMENT_3D ( 'NONE', #2533, #4662, #835 ) ;
#4093=PRODUCT_DEFINITION_CONTEXT ( 'detailed design', #3109, 'design' ) ;
#4095=VECTOR ( 'NONE', #4814, 1000.000000000000000 ) ;
#4096=ORIENTED_EDGE ( 'NONE', *, *, #794, .T. ) ;
#4104=ORIENTED_EDGE ( 'NONE', *, *, #1301, .F. ) ;
#4111=DIRECTION ( 'NONE',  ( -1.000000000000000000, -0.000000000000000000, -0.000000000000000000 ) ) ;
#4135=DIRECTION ( 'NONE',  ( 0.000000000000000000, -1.000000000000000000, 1.188187522481193495E-15 ) ) ;
#4144=VECTOR ( 'NONE', #1179, 1000.000000000000000 ) ;
#4148=AXIS2_PLACEMENT_3D ( 'NONE', #4665, #2194, #4295 ) ;
#4154=AXIS2_PLACEMENT_3D ( 'NONE', #2434, #5290, #769 ) ;
#4162=CARTESIAN_POINT ( 'NONE',  ( 0.6000000000000033085, 0.000000000000000000, 0.000000000000000000 ) ) ;
#4170=CARTESIAN_POINT ( 'NONE',  ( 6.000000000000000000, 6.193651186687738874E-16, -5.057500000000000107 ) ) ;
#4171=ORIENTED_EDGE ( 'NONE', *, *, #5313, .F. ) ;
#4176=ADVANCED_BREP_SHAPE_REPRESENTATION ( '', ( #1819, #4154 ), #2853 ) ;
#4177=ORIENTED_EDGE ( 'NONE', *, *, #1959, .F. ) ;
#4185=CARTESIAN_POINT ( 'NONE',  ( 0.000000000000000000, -2.919948986426526893, 5.057500000000001883 ) ) ;
#4194=CARTESIAN_POINT ( 'NONE',  ( 0.000000000000000000, 2.919948986426526005, -5.057500000000002771 ) ) ;
#4196=EDGE_CURVE ( 'NONE', #5142, #1861, #4848, .T. ) ;
#4197=ORIENTED_EDGE ( 'NONE', *, *, #1491, .T. ) ;
#4210=EDGE_LOOP ( 'NONE', ( #153, #2513 ) ) ;
#4216=FACE_OUTER_BOUND ( 'NONE', #44, .T. ) ;
#4223=CARTESIAN_POINT ( 'NONE',  ( 6.000000000000000000, -2.919948986426526893, 5.057500000000001883 ) ) ;
#4229=ORIENTED_EDGE ( 'NONE', *, *, #817, .T. ) ;
#4238=MECHANICAL_DESIGN_GEOMETRIC_PRESENTATION_REPRESENTATION('',(#2138),#916);
#4241=ORIENTED_EDGE ( 'NONE', *, *, #609, .F. ) ;
#4244=CARTESIAN_POINT ( 'NONE',  ( 92.00000000000000000, 6.757601037695095565E-16, -5.035999999999999588 ) ) ;
#4246=VERTEX_POINT ( 'NONE', #4534 ) ;
#4269=DIRECTION ( 'NONE',  ( 0.000000000000000000, 0.4999999999999990008, -0.8660254037844392627 ) ) ;
#4274=DIRECTION ( 'NONE',  ( 1.000000000000000000, 0.000000000000000000, 0.000000000000000000 ) ) ;
#4293=CARTESIAN_POINT ( 'NONE',  ( 6.000000000000000000, -4.379923479639802331, -2.528749999999995612 ) ) ;
#4295=DIRECTION ( 'NONE',  ( 0.000000000000000000, 0.000000000000000000, -1.000000000000000000 ) ) ;
#4297=EDGE_CURVE ( 'NONE', #5294, #4433, #2830, .T. ) ;
#4312=CIRCLE ( 'NONE', #644, 5.057500000000000107 ) ;
#4324=FACE_OUTER_BOUND ( 'NONE', #2927, .T. ) ;
#4326=AXIS2_PLACEMENT_3D ( 'NONE', #5332, #784, #2893 ) ;
#4331=DIRECTION ( 'NONE',  ( -1.000000000000000000, -0.000000000000000000, -0.000000000000000000 ) ) ;
#4339=DIRECTION ( 'NONE',  ( -1.000000000000000000, -0.000000000000000000, -0.000000000000000000 ) ) ;
#4341=EDGE_CURVE ( 'NONE', #1489, #5294, #5059, .T. ) ;
#4364=DIRECTION ( 'NONE',  ( -1.000000000000000000, -0.000000000000000000, -0.000000000000000000 ) ) ;
#4367=CARTESIAN_POINT ( 'NONE',  ( 91.03600000000004400, 0.000000000000000000, 6.000000000000000888 ) ) ;
#4380=AXIS2_PLACEMENT_3D ( 'NONE', #4723, #243, #1484 ) ;
#4382=ORIENTED_EDGE ( 'NONE', *, *, #5006, .T. ) ;
#4383=DIRECTION ( 'NONE',  ( 0.000000000000000000, 0.000000000000000000, 1.000000000000000000 ) ) ;
#4387=AXIS2_PLACEMENT_3D ( 'NONE', #5145, #1894, #3133 ) ;
#4402=ADVANCED_FACE ( 'NONE', ( #866 ), #2972, .T. ) ;
#4403=VECTOR ( 'NONE', #3123, 1000.000000000000227 ) ;
#4410=ORIENTED_EDGE ( 'NONE', *, *, #1253, .F. ) ;
#4416=SHAPE_DEFINITION_REPRESENTATION ( #1810, #2934 ) ;
#4417=CARTESIAN_POINT ( 'NONE',  ( -31.74999999999995737, 7.347880794884121708E-16, -6.000000000000001776 ) ) ;
#4422=DIRECTION ( 'NONE',  ( -1.000000000000000000, -0.000000000000000000, -0.000000000000000000 ) ) ;
#4423=LINE ( 'NONE', #389, #3557 ) ;
#4433=VERTEX_POINT ( 'NONE', #605 ) ;
#4436=FACE_OUTER_BOUND ( 'NONE', #3742, .T. ) ;
#4444=ORIENTED_EDGE ( 'NONE', *, *, #3576, .F. ) ;
#4452=CARTESIAN_POINT ( 'NONE',  ( 6.000000000000000000, 2.919948986426526005, -5.057500000000002771 ) ) ;
#4457=VERTEX_POINT ( 'NONE', #630 ) ;
#4460=ORIENTED_EDGE ( 'NONE', *, *, #2896, .T. ) ;
#4467=DIRECTION ( 'NONE',  ( 1.000000000000000000, 0.000000000000000000, 0.000000000000000000 ) ) ;
#4470=CARTESIAN_POINT ( 'NONE',  ( 92.00000000000000000, 0.000000000000000000, 0.000000000000000000 ) ) ;
#4476=DIRECTION ( 'NONE',  ( 0.000000000000000000, -1.000000000000000000, 1.039664082171044284E-15 ) ) ;
#4480=VERTEX_POINT ( 'NONE', #4293 ) ;
#4484=DIRECTION ( 'NONE',  ( -1.000000000000000000, 0.000000000000000000, -0.000000000000000000 ) ) ;
#4504=DIRECTION ( 'NONE',  ( 1.000000000000000000, 0.000000000000000000, 0.000000000000000000 ) ) ;
#4517=PRODUCT_DEFINITION ( 'UNKNOWN', '', #2053, #4093 ) ;
#4519=DIRECTION ( 'NONE',  ( 1.000000000000000000, 0.000000000000000000, 0.000000000000000000 ) ) ;
#4524=CARTESIAN_POINT ( 'NONE',  ( 6.000000000000000000, 0.000000000000000000, 0.000000000000000000 ) ) ;
#4529=EDGE_CURVE ( 'NONE', #1888, #2898, #1884, .T. ) ;
#4531=VECTOR ( 'NONE', #1907, 1000.000000000000114 ) ;
#4534=CARTESIAN_POINT ( 'NONE',  ( 6.000000000000000000, 2.919948986426538440, 5.057499999999994778 ) ) ;
#4542=DIRECTION ( 'NONE',  ( -1.000000000000000000, -0.000000000000000000, -0.000000000000000000 ) ) ;
#4546=ADVANCED_FACE ( 'NONE', ( #1070 ), #2241, .T. ) ;
#4555=VERTEX_POINT ( 'NONE', #3563 ) ;
#4585=ORIENTED_EDGE ( 'NONE', *, *, #365, .F. ) ;
#4586=CARTESIAN_POINT ( 'NONE',  ( 0.000000000000000000, 0.000000000000000000, 0.000000000000000000 ) ) ;
#4589=ORIENTED_EDGE ( 'NONE', *, *, #1387, .F. ) ;
#4592=ORIENTED_EDGE ( 'NONE', *, *, #4931, .T. ) ;
#4594=DIRECTION ( 'NONE',  ( 0.000000000000000000, 0.4999999999999991118, -0.8660254037844391517 ) ) ;
#4595=VERTEX_POINT ( 'NONE', #3294 ) ;
#4603=EDGE_LOOP ( 'NONE', ( #2908, #4229, #4171, #792 ) ) ;
#4634=AXIS2_PLACEMENT_3D ( 'NONE', #1087, #1118, #3930 ) ;
#4637=CIRCLE ( 'NONE', #2300, 6.600000000000001421 ) ;
#4639=STYLED_ITEM('',(#5433),#1819);
#4641=ADVANCED_FACE ( 'NONE', ( #1957 ), #1608, .F. ) ;
#4649=DIRECTION ( 'NONE',  ( 0.000000000000000000, 0.000000000000000000, -1.000000000000000000 ) ) ;
#4654=VECTOR ( 'NONE', #1289, 1000.000000000000000 ) ;
#4656=EDGE_CURVE ( 'NONE', #3300, #2868, #4423, .T. ) ;
#4662=DIRECTION ( 'NONE',  ( -0.000000000000000000, 0.8660254037844392627, 0.4999999999999989453 ) ) ;
#4665=CARTESIAN_POINT ( 'NONE',  ( 0.6000000000000033085, 0.000000000000000000, 8.400000000000000355 ) ) ;
#4683=CARTESIAN_POINT ( 'NONE',  ( 0.000000000000000000, 5.839897972853065333, -6.938893903907228378E-15 ) ) ;
#4684=CARTESIAN_POINT ( 'NONE',  ( 6.000000000000000000, 5.839897972853065333, -6.938893903907228378E-15 ) ) ;
#4688=CARTESIAN_POINT ( 'NONE',  ( 6.000000000000000000, 5.839897972853065333, -6.938893903907228378E-15 ) ) ;
#4689=ORIENTED_EDGE ( 'NONE', *, *, #961, .F. ) ;
#4698=EDGE_CURVE ( 'NONE', #3352, #3274, #3206, .T. ) ;
#4712=ADVANCED_FACE ( 'NONE', ( #1965 ), #3656, .F. ) ;
#4720=AXIS2_PLACEMENT_3D ( 'NONE', #559, #994, #2045 ) ;
#4723=CARTESIAN_POINT ( 'NONE',  ( 91.03600000000004400, 0.000000000000000000, 0.000000000000000000 ) ) ;
#4728=( NAMED_UNIT ( * ) PLANE_ANGLE_UNIT ( ) SI_UNIT ( $, .RADIAN. ) );
#4736=CARTESIAN_POINT ( 'NONE',  ( 6.000000000000000000, 2.919948986426538440, 5.057499999999994778 ) ) ;
#4740=AXIS2_PLACEMENT_3D ( 'NONE', #4162, #2125, #3831 ) ;
#4747=ORIENTED_EDGE ( 'NONE', *, *, #2662, .F. ) ;
#4753=EDGE_LOOP ( 'NONE', ( #2616, #329, #3213 ) ) ;
#4777=ORIENTED_EDGE ( 'NONE', *, *, #609, .T. ) ;
#4783=ORIENTED_EDGE ( 'NONE', *, *, #3699, .F. ) ;
#4793=DIRECTION ( 'NONE',  ( 1.000000000000000000, 0.000000000000000000, 0.000000000000000000 ) ) ;
#4798=DIRECTION ( 'NONE',  ( 0.000000000000000000, 0.8660254037844379305, -0.5000000000000012212 ) ) ;
#4813=CARTESIAN_POINT ( 'NONE',  ( 6.000000000000000000, -2.919948986426526893, 5.057500000000001883 ) ) ;
#4814=DIRECTION ( 'NONE',  ( -0.5000000000000046629, 0.000000000000000000, 0.8660254037844359321 ) ) ;
#4815=CIRCLE ( 'NONE', #2210, 6.000000000000001776 ) ;
#4820=DIRECTION ( 'NONE',  ( 0.000000000000000000, 0.000000000000000000, 1.000000000000000000 ) ) ;
#4834=CIRCLE ( 'NONE', #5284, 5.057500000000000107 ) ;
#4847=LINE ( 'NONE', #3609, #4095 ) ;
#4848=CIRCLE ( 'NONE', #2152, 0.5999999999999998668 ) ;
#4852=ORIENTED_EDGE ( 'NONE', *, *, #940, .T. ) ;
#4862=FACE_BOUND ( 'NONE', #3083, .T. ) ;
#4868=EDGE_LOOP ( 'NONE', ( #5168, #1520 ) ) ;
#4880=PLANE ( 'NONE',  #304 ) ;
#4888=ORIENTED_EDGE ( 'NONE', *, *, #2069, .T. ) ;
#4895=DIRECTION ( 'NONE',  ( 1.000000000000000000, 0.000000000000000000, 0.000000000000000000 ) ) ;
#4910=DIRECTION ( 'NONE',  ( -1.000000000000000000, -0.000000000000000000, -0.000000000000000000 ) ) ;
#4913=EDGE_LOOP ( 'NONE', ( #1857, #3929, #5119 ) ) ;
#4916=( GEOMETRIC_REPRESENTATION_CONTEXT ( 3 ) GLOBAL_UNCERTAINTY_ASSIGNED_CONTEXT ( ( #2377 ) ) GLOBAL_UNIT_ASSIGNED_CONTEXT ( ( #1538, #704, #178 ) ) REPRESENTATION_CONTEXT ( 'NONE', 'WORKASPACE' ) );
#4926=CONICAL_SURFACE ( 'NONE', #3978, 5.035999999999999588, 0.7853981633974743692 ) ;
#4929=VERTEX_POINT ( 'NONE', #2238 ) ;
#4931=EDGE_CURVE ( 'NONE', #3733, #4457, #1063, .T. ) ;
#4940=CARTESIAN_POINT ( 'NONE',  ( 6.000000000000000000, -2.919948986426526893, 5.057500000000001883 ) ) ;
#4942=PLANE ( 'NONE',  #661 ) ;
#4952=ORIENTED_EDGE ( 'NONE', *, *, #69, .F. ) ;
#4957=ORIENTED_EDGE ( 'NONE', *, *, #352, .T. ) ;
#4960=CARTESIAN_POINT ( 'NONE',  ( 12.59999999999999964, 0.000000000000000000, 0.000000000000000000 ) ) ;
#4966=DIRECTION ( 'NONE',  ( 0.000000000000000000, 0.000000000000000000, 1.000000000000000000 ) ) ;
#4968=CARTESIAN_POINT ( 'NONE',  ( 6.000000000000000000, 4.379923479639800554, 2.528749999999996056 ) ) ;
#4986=ORIENTED_EDGE ( 'NONE', *, *, #787, .F. ) ;
#5005=ORIENTED_EDGE ( 'NONE', *, *, #4297, .F. ) ;
#5006=EDGE_CURVE ( 'NONE', #1489, #3274, #4847, .T. ) ;
#5014=AXIS2_PLACEMENT_3D ( 'NONE', #4586, #4484, #4068 ) ;
#5017=CARTESIAN_POINT ( 'NONE',  ( 12.59999999999999964, 0.000000000000000000, 0.000000000000000000 ) ) ;
#5024=DIRECTION ( 'NONE',  ( 0.000000000000000000, 0.4999999999999990008, -0.8660254037844392627 ) ) ;
#5025=DIRECTION ( 'NONE',  ( 0.000000000000000000, 1.000000000000000000, -1.188187522481193495E-15 ) ) ;
#5031=( LENGTH_UNIT ( ) NAMED_UNIT ( * ) SI_UNIT ( .MILLI., .METRE. ) );
#5036=ORIENTED_EDGE ( 'NONE', *, *, #2727, .F. ) ;
#5051=ORIENTED_EDGE ( 'NONE', *, *, #631, .F. ) ;
#5054=EDGE_CURVE ( 'NONE', #4929, #2539, #1637, .T. ) ;
#5059=LINE ( 'NONE', #4170, #1110 ) ;
#5083=AXIS2_PLACEMENT_3D ( 'NONE', #3606, #1004, #4383 ) ;
#5091=CARTESIAN_POINT ( 'NONE',  ( 6.000000000000000000, 5.839897972853065333, -6.938893903907228378E-15 ) ) ;
#5092=VECTOR ( 'NONE', #4269, 1000.000000000000000 ) ;
#5098=FACE_OUTER_BOUND ( 'NONE', #1187, .T. ) ;
#5105=EDGE_CURVE ( 'NONE', #5294, #4480, #3212, .T. ) ;
#5108=LINE ( 'NONE', #1365, #3584 ) ;
#5119=ORIENTED_EDGE ( 'NONE', *, *, #2896, .F. ) ;
#5120=PLANE ( 'NONE',  #4720 ) ;
#5126=CARTESIAN_POINT ( 'NONE',  ( 6.000000000000000000, 0.000000000000000000, 0.000000000000000000 ) ) ;
#5130=( LENGTH_UNIT ( ) NAMED_UNIT ( * ) SI_UNIT ( .MILLI., .METRE. ) );
#5131=ORIENTED_EDGE ( 'NONE', *, *, #4341, .T. ) ;
#5136=LINE ( 'NONE', #4736, #314 ) ;
#5142=VERTEX_POINT ( 'NONE', #3316 ) ;
#5145=CARTESIAN_POINT ( 'NONE',  ( 6.000000000000000000, 0.000000000000000000, 0.000000000000000000 ) ) ;
#5147=ORIENTED_EDGE ( 'NONE', *, *, #1528, .T. ) ;
#5157=CARTESIAN_POINT ( 'NONE',  ( 6.000000000000000000, 5.839897972853065333, -6.938893903907228378E-15 ) ) ;
#5159=LINE ( 'NONE', #1441, #4403 ) ;
#5168=ORIENTED_EDGE ( 'NONE', *, *, #5313, .T. ) ;
#5181=ADVANCED_FACE ( 'NONE', ( #461 ), #1715, .T. ) ;
#5183=AXIS2_PLACEMENT_3D ( 'NONE', #3187, #4895, #678 ) ;
#5184=EDGE_CURVE ( 'NONE', #1888, #2103, #1818, .T. ) ;
#5185=DIRECTION ( 'NONE',  ( 0.000000000000000000, 0.000000000000000000, -1.000000000000000000 ) ) ;
#5202=ORIENTED_EDGE ( 'NONE', *, *, #1202, .T. ) ;
#5210=CIRCLE ( 'NONE', #3826, 8.400000000000000355 ) ;
#5221=CARTESIAN_POINT ( 'NONE',  ( 6.000000000000000000, 5.839897972853065333, -6.938893903907228378E-15 ) ) ;
#5231=VECTOR ( 'NONE', #2214, 1000.000000000000000 ) ;
#5232=EDGE_LOOP ( 'NONE', ( #4957, #2287, #370, #3794 ) ) ;
#5246=LINE ( 'NONE', #4417, #46 ) ;
#5250=CARTESIAN_POINT ( 'NONE',  ( 6.000000000000000000, 5.839897972853065333, -6.938893903907228378E-15 ) ) ;
#5268=ADVANCED_FACE ( 'NONE', ( #2675 ), #1760, .T. ) ;
#5284=AXIS2_PLACEMENT_3D ( 'NONE', #785, #3233, #2798 ) ;
#5290=DIRECTION ( 'NONE',  ( 0.000000000000000000, 0.000000000000000000, 1.000000000000000000 ) ) ;
#5293=CIRCLE ( 'NONE', #1711, 5.057500000000000107 ) ;
#5294=VERTEX_POINT ( 'NONE', #159 ) ;
#5303=AXIS2_PLACEMENT_3D ( 'NONE', #3227, #1146, #740 ) ;
#5310=ORIENTED_EDGE ( 'NONE', *, *, #1594, .F. ) ;
#5313=EDGE_CURVE ( 'NONE', #366, #4555, #5210, .T. ) ;
#5332=CARTESIAN_POINT ( 'NONE',  ( -31.74999999999995737, 0.000000000000000000, 0.000000000000000000 ) ) ;
#5344=ORIENTED_EDGE ( 'NONE', *, *, #1959, .T. ) ;
#5351=CIRCLE ( 'NONE', #4380, 6.000000000000000888 ) ;
#5359=MECHANICAL_DESIGN_GEOMETRIC_PRESENTATION_REPRESENTATION('',(#4639),#4916);
#5366=ORIENTED_EDGE ( 'NONE', *, *, #817, .F. ) ;
#5367=EDGE_LOOP ( 'NONE', ( #27, #2948 ) ) ;
#5427=COLOUR_RGB('Black',0.12,0.14,0.17);
#5428=FILL_AREA_STYLE_COLOUR('',#5427);
#5429=FILL_AREA_STYLE('',(#5428));
#5430=SURFACE_STYLE_FILL_AREA(#5429);
#5431=SURFACE_SIDE_STYLE('',(#5430));
#5432=SURFACE_STYLE_USAGE(.BOTH.,#5431);
#5433=PRESENTATION_STYLE_ASSIGNMENT((#5432));
ENDSEC;
END-ISO-10303-21;
